ISO-10303-21;
HEADER;
FILE_DESCRIPTION (('STEP AP203'),
    '1' );
FILE_NAME ('bench vise4-.step',
    '2026-10-07T23:37:23',
    ( '' ),
    ( '' ),
    'SwSTEP 2.0',
    'SolidWorks 2024',
    '' );
FILE_SCHEMA (( 'AUTOMOTIVE_DESIGN' ));
ENDSEC;

DATA;
#4=CARTESIAN_POINT ( 'NONE',  ( 2.740000000000000213, 8.729000000000002757, 3.333750000000001990 ) ) ;
#100=PRODUCT_DEFINITION_SHAPE ( 'NONE', 'NONE',  #1914 ) ;
#134=ORIENTED_EDGE ( 'NONE', *, *, #3696, .T. ) ;
#136=CARTESIAN_POINT ( 'NONE',  ( -2.740000000000000657, 7.974000000000001087, 3.323750000000001759 ) ) ;
#142=DIRECTION ( 'NONE',  ( 0.7071067811865475727, 0.7071067811865475727, -0.000000000000000000 ) ) ;
#151=DIRECTION ( 'NONE',  ( 0.5773502691896258421, -0.5773502691896258421, -0.5773502691896258421 ) ) ;
#186=CARTESIAN_POINT ( 'NONE',  ( 2.750000000000000888, 7.964000000000000412, 3.823750000000002647 ) ) ;
#187=EDGE_CURVE ( 'NONE', #3123, #5331, #5845, .T. ) ;
#211=AXIS2_PLACEMENT_3D ( 'NONE', #382, #6663, #1045 ) ;
#223=VECTOR ( 'NONE', #5347, 39.37007874015748854 ) ;
#226=ADVANCED_FACE ( 'NONE', ( #3542 ), #7853, .F. ) ;
#282=DIRECTION ( 'NONE',  ( -1.000000000000000000, 0.000000000000000000, 0.000000000000000000 ) ) ;
#297=DIRECTION ( 'NONE',  ( 0.000000000000000000, 0.000000000000000000, -1.000000000000000000 ) ) ;
#305=DIRECTION ( 'NONE',  ( 0.000000000000000000, -1.000000000000000000, 0.000000000000000000 ) ) ;
#323=VECTOR ( 'NONE', #3923, 39.37007874015748143 ) ;
#358=LINE ( 'NONE', #2860, #223 ) ;
#369=CARTESIAN_POINT ( 'NONE',  ( -2.740000000000000657, 7.964000000000000412, 3.333750000000001990 ) ) ;
#376=CARTESIAN_POINT ( 'NONE',  ( -2.740000000000000657, 7.964000000000000412, 3.333750000000001990 ) ) ;
#382=CARTESIAN_POINT ( 'NONE',  ( -2.750000000000000444, 8.729000000000002757, 3.823750000000002647 ) ) ;
#384=LINE ( 'NONE', #2356, #6978 ) ;
#389=DIRECTION ( 'NONE',  ( -0.5773502691896258421, -0.5773502691896258421, 0.5773502691896258421 ) ) ;
#396=EDGE_LOOP ( 'NONE', ( #4747, #7145, #8060, #3804 ) ) ;
#402=VERTEX_POINT ( 'NONE', #2400 ) ;
#419=LINE ( 'NONE', #7964, #7254 ) ;
#423=CARTESIAN_POINT ( 'NONE',  ( 2.750000000000000888, 7.974000000000001087, 3.823750000000002647 ) ) ;
#436=ORIENTED_EDGE ( 'NONE', *, *, #3533, .T. ) ;
#447=VECTOR ( 'NONE', #1168, 39.37007874015748854 ) ;
#449=PRODUCT_DEFINITION_FORMATION_WITH_SPECIFIED_SOURCE ( 'ANY', '', #6746, .NOT_KNOWN. ) ;
#465=ORIENTED_EDGE ( 'NONE', *, *, #3392, .T. ) ;
#470=AXIS2_PLACEMENT_3D ( 'NONE', #4283, #3546, #7983 ) ;
#476=EDGE_CURVE ( 'NONE', #1089, #3668, #7630, .T. ) ;
#497=FACE_OUTER_BOUND ( 'NONE', #7617, .T. ) ;
#506=DIRECTION ( 'NONE',  ( 1.000000000000000000, 0.000000000000000000, 0.000000000000000000 ) ) ;
#507=ORIENTED_EDGE ( 'NONE', *, *, #7374, .F. ) ;
#509=LINE ( 'NONE', #3000, #6718 ) ;
#526=ADVANCED_FACE ( 'NONE', ( #5172 ), #6456, .T. ) ;
#545=EDGE_LOOP ( 'NONE', ( #2469, #1170, #5240, #4840 ) ) ;
#582=CARTESIAN_POINT ( 'NONE',  ( 2.740000000000000657, 7.964000000000000412, 3.813750000000002416 ) ) ;
#590=ADVANCED_FACE ( 'NONE', ( #4094 ), #4020, .T. ) ;
#619=VECTOR ( 'NONE', #1796, 39.37007874015748143 ) ;
#622=ORIENTED_EDGE ( 'NONE', *, *, #4822, .F. ) ;
#623=CARTESIAN_POINT ( 'NONE',  ( 2.750000000000000888, 7.974000000000001087, 3.333750000000001990 ) ) ;
#625=DIRECTION ( 'NONE',  ( 0.000000000000000000, -0.000000000000000000, 1.000000000000000000 ) ) ;
#636=ORIENTED_EDGE ( 'NONE', *, *, #2488, .F. ) ;
#651=CARTESIAN_POINT ( 'NONE',  ( 2.750000000000000888, 8.719000000000001194, 3.823750000000002647 ) ) ;
#658=DIRECTION ( 'NONE',  ( 0.7071067811865474617, 0.000000000000000000, -0.7071067811865474617 ) ) ;
#664=ORIENTED_EDGE ( 'NONE', *, *, #7776, .T. ) ;
#699=ADVANCED_FACE ( 'NONE', ( #7242 ), #3421, .T. ) ;
#701=VECTOR ( 'NONE', #8015, 39.37007874015748143 ) ;
#707=LINE ( 'NONE', #751, #5136 ) ;
#732=ORIENTED_EDGE ( 'NONE', *, *, #1330, .F. ) ;
#751=CARTESIAN_POINT ( 'NONE',  ( -2.750000000000000888, 8.719000000000001194, 3.823750000000002647 ) ) ;
#757=LINE ( 'NONE', #6249, #7160 ) ;
#780=PLANE ( 'NONE',  #6507 ) ;
#822=VERTEX_POINT ( 'NONE', #582 ) ;
#834=ORIENTED_EDGE ( 'NONE', *, *, #5371, .T. ) ;
#842=DIRECTION ( 'NONE',  ( 0.000000000000000000, 0.000000000000000000, 1.000000000000000000 ) ) ;
#848=DIRECTION ( 'NONE',  ( -0.000000000000000000, 0.7071067811865475727, 0.7071067811865475727 ) ) ;
#886=ORIENTED_EDGE ( 'NONE', *, *, #5427, .F. ) ;
#902=DIRECTION ( 'NONE',  ( -7.142086257945775577E-16, -1.000000000000000000, 0.000000000000000000 ) ) ;
#942=EDGE_CURVE ( 'NONE', #1477, #5222, #5980, .T. ) ;
#958=DIRECTION ( 'NONE',  ( -0.7071067811865554553, 1.583668658704876446E-14, -0.7071067811865395791 ) ) ;
#963=VERTEX_POINT ( 'NONE', #7388 ) ;
#970=VECTOR ( 'NONE', #2759, 39.37007874015748143 ) ;
#971=DIRECTION ( 'NONE',  ( 0.7071067811865395791, -5.050217624812654886E-16, 0.7071067811865554553 ) ) ;
#1005=EDGE_CURVE ( 'NONE', #1089, #4859, #358, .T. ) ;
#1010=CARTESIAN_POINT ( 'NONE',  ( -2.750000000000000888, 7.964000000000000412, 3.333750000000001990 ) ) ;
#1036=( NAMED_UNIT ( * ) SI_UNIT ( $, .STERADIAN. ) SOLID_ANGLE_UNIT ( ) );
#1045=DIRECTION ( 'NONE',  ( 0.000000000000000000, -0.000000000000000000, 1.000000000000000000 ) ) ;
#1046=CARTESIAN_POINT ( 'NONE',  ( 2.745000000000000995, 7.974000000000001087, 3.818750000000002753 ) ) ;
#1064=DIRECTION ( 'NONE',  ( 0.000000000000000000, -0.7071067811865475727, 0.7071067811865475727 ) ) ;
#1089=VERTEX_POINT ( 'NONE', #4 ) ;
#1091=PLANE ( 'NONE',  #470 ) ;
#1099=CARTESIAN_POINT ( 'NONE',  ( -2.740000000000000213, 8.719000000000001194, 3.323750000000001759 ) ) ;
#1100=ORIENTED_EDGE ( 'NONE', *, *, #4193, .T. ) ;
#1120=( GEOMETRIC_REPRESENTATION_CONTEXT ( 3 ) GLOBAL_UNCERTAINTY_ASSIGNED_CONTEXT ( ( #4051 ) ) GLOBAL_UNIT_ASSIGNED_CONTEXT ( ( #5826, #3965, #1036 ) ) REPRESENTATION_CONTEXT ( 'NONE', 'WORKASPACE' ) );
#1126=ORIENTED_EDGE ( 'NONE', *, *, #5708, .F. ) ;
#1131=CARTESIAN_POINT ( 'NONE',  ( 2.750000000000000888, 8.719000000000001194, 3.333750000000001990 ) ) ;
#1138=ORIENTED_EDGE ( 'NONE', *, *, #1704, .F. ) ;
#1140=LINE ( 'NONE', #1863, #619 ) ;
#1168=DIRECTION ( 'NONE',  ( 0.7071067811865474617, 0.000000000000000000, 0.7071067811865474617 ) ) ;
#1170=ORIENTED_EDGE ( 'NONE', *, *, #4265, .T. ) ;
#1184=CARTESIAN_POINT ( 'NONE',  ( 2.750000000000000888, 8.719000000000001194, 3.813750000000002416 ) ) ;
#1199=EDGE_LOOP ( 'NONE', ( #834, #3338, #3920, #5891 ) ) ;
#1204=ORIENTED_EDGE ( 'NONE', *, *, #3096, .F. ) ;
#1212=ORIENTED_EDGE ( 'NONE', *, *, #7776, .F. ) ;
#1219=PLANE ( 'NONE',  #7547 ) ;
#1220=FACE_OUTER_BOUND ( 'NONE', #1749, .T. ) ;
#1255=VECTOR ( 'NONE', #7754, 39.37007874015748854 ) ;
#1262=AXIS2_PLACEMENT_3D ( 'NONE', #6941, #7714, #2068 ) ;
#1267=DIRECTION ( 'NONE',  ( 0.000000000000000000, 0.000000000000000000, -1.000000000000000000 ) ) ;
#1268=CARTESIAN_POINT ( 'NONE',  ( 2.740000000000000657, 7.964000000000000412, 3.813750000000002416 ) ) ;
#1273=DIRECTION ( 'NONE',  ( -7.142086257945775577E-16, -1.000000000000000000, 0.000000000000000000 ) ) ;
#1330=EDGE_CURVE ( 'NONE', #6945, #3927, #4841, .T. ) ;
#1338=DIRECTION ( 'NONE',  ( 0.000000000000000000, -1.000000000000000000, 0.000000000000000000 ) ) ;
#1370=AXIS2_PLACEMENT_3D ( 'NONE', #369, #7140, #3528 ) ;
#1387=PLANE ( 'NONE',  #7970 ) ;
#1426=EDGE_CURVE ( 'NONE', #6692, #6736, #4174, .T. ) ;
#1454=ADVANCED_FACE ( 'NONE', ( #4423 ), #3773, .T. ) ;
#1477=VERTEX_POINT ( 'NONE', #623 ) ;
#1518=DIRECTION ( 'NONE',  ( 0.000000000000000000, 0.7071067811865475727, 0.7071067811865475727 ) ) ;
#1523=EDGE_CURVE ( 'NONE', #6692, #5123, #3124, .T. ) ;
#1537=AXIS2_PLACEMENT_3D ( 'NONE', #5300, #848, #2204 ) ;
#1546=DIRECTION ( 'NONE',  ( 0.000000000000000000, -1.000000000000000000, 0.000000000000000000 ) ) ;
#1550=EDGE_CURVE ( 'NONE', #8018, #7102, #6186, .T. ) ;
#1569=ORIENTED_EDGE ( 'NONE', *, *, #1779, .T. ) ;
#1573=CARTESIAN_POINT ( 'NONE',  ( 2.750000000000000888, 7.974000000000001087, 3.823750000000002647 ) ) ;
#1594=CARTESIAN_POINT ( 'NONE',  ( 2.750000000000000888, 8.729000000000002757, 3.333750000000001990 ) ) ;
#1658=VECTOR ( 'NONE', #902, 39.37007874015748143 ) ;
#1665=AXIS2_PLACEMENT_3D ( 'NONE', #5595, #2410, #6825 ) ;
#1679=LINE ( 'NONE', #6613, #6208 ) ;
#1704=EDGE_CURVE ( 'NONE', #5031, #963, #6531, .T. ) ;
#1713=ORIENTED_EDGE ( 'NONE', *, *, #1523, .F. ) ;
#1716=ORIENTED_EDGE ( 'NONE', *, *, #1779, .F. ) ;
#1729=ADVANCED_FACE ( 'NONE', ( #4546 ), #780, .T. ) ;
#1731=CARTESIAN_POINT ( 'NONE',  ( 2.750000000000000888, 8.719000000000001194, 3.823750000000002647 ) ) ;
#1749=EDGE_LOOP ( 'NONE', ( #3009, #5625, #1716 ) ) ;
#1761=DIRECTION ( 'NONE',  ( 0.5773502691896152950, 0.5773502691896467143, 0.5773502691896152950 ) ) ;
#1769=EDGE_LOOP ( 'NONE', ( #5268, #3911, #4916 ) ) ;
#1776=LINE ( 'NONE', #5529, #7957 ) ;
#1779=EDGE_CURVE ( 'NONE', #4445, #5331, #6765, .T. ) ;
#1782=PLANE ( 'NONE',  #4212 ) ;
#1784=ADVANCED_FACE ( 'NONE', ( #1220 ), #4949, .T. ) ;
#1787=PLANE ( 'NONE',  #6991 ) ;
#1796=DIRECTION ( 'NONE',  ( 1.000000000000000000, 0.000000000000000000, 0.000000000000000000 ) ) ;
#1808=ORIENTED_EDGE ( 'NONE', *, *, #7675, .F. ) ;
#1815=ORIENTED_EDGE ( 'NONE', *, *, #6447, .F. ) ;
#1820=ORIENTED_EDGE ( 'NONE', *, *, #3088, .T. ) ;
#1847=ORIENTED_EDGE ( 'NONE', *, *, #1005, .T. ) ;
#1851=LINE ( 'NONE', #7852, #5531 ) ;
#1855=DIRECTION ( 'NONE',  ( 0.000000000000000000, 0.000000000000000000, 1.000000000000000000 ) ) ;
#1858=ADVANCED_FACE ( 'NONE', ( #6264 ), #4988, .F. ) ;
#1863=CARTESIAN_POINT ( 'NONE',  ( 0.000000000000000000, 8.719000000000001194, 3.323750000000001759 ) ) ;
#1879=CARTESIAN_POINT ( 'NONE',  ( -2.750000000000000888, 7.964000000000000412, 3.813750000000002416 ) ) ;
#1885=EDGE_LOOP ( 'NONE', ( #5087, #6100, #4600, #6602 ) ) ;
#1886=VECTOR ( 'NONE', #2351, 39.37007874015748854 ) ;
#1910=AXIS2_PLACEMENT_3D ( 'NONE', #4811, #4143, #4185 ) ;
#1914=PRODUCT_DEFINITION ( 'UNKNOWN', '', #449, #2909 ) ;
#1928=ORIENTED_EDGE ( 'NONE', *, *, #4278, .F. ) ;
#1961=DIRECTION ( 'NONE',  ( -0.7071067811865395791, 5.050217624812654886E-16, 0.7071067811865554553 ) ) ;
#1963=CARTESIAN_POINT ( 'NONE',  ( 2.750000000000000888, 8.719000000000001194, 3.333750000000001990 ) ) ;
#2011=CARTESIAN_POINT ( 'NONE',  ( -2.745000000000000551, 8.724000000000001975, 3.333750000000001990 ) ) ;
#2013=CARTESIAN_POINT ( 'NONE',  ( 2.750000000000000888, 8.729000000000002757, 3.813750000000002416 ) ) ;
#2022=VECTOR ( 'NONE', #1546, 39.37007874015748143 ) ;
#2048=LINE ( 'NONE', #5689, #2419 ) ;
#2060=VECTOR ( 'NONE', #5021, 39.37007874015748854 ) ;
#2068=DIRECTION ( 'NONE',  ( -0.7071067811865474617, 0.000000000000000000, 0.7071067811865474617 ) ) ;
#2071=ORIENTED_EDGE ( 'NONE', *, *, #476, .T. ) ;
#2110=ADVANCED_FACE ( 'NONE', ( #6866 ), #6210, .T. ) ;
#2123=ORIENTED_EDGE ( 'NONE', *, *, #5558, .F. ) ;
#2128=ORIENTED_EDGE ( 'NONE', *, *, #4762, .T. ) ;
#2160=DIRECTION ( 'NONE',  ( 1.000000000000000000, 0.000000000000000000, 0.000000000000000000 ) ) ;
#2190=LINE ( 'NONE', #1573, #3581 ) ;
#2192=EDGE_CURVE ( 'NONE', #5123, #3668, #1140, .T. ) ;
#2204=DIRECTION ( 'NONE',  ( 1.000000000000000000, 0.000000000000000000, 0.000000000000000000 ) ) ;
#2232=CARTESIAN_POINT ( 'NONE',  ( 2.740000000000000657, 8.729000000000002757, 3.823750000000002647 ) ) ;
#2234=CARTESIAN_POINT ( 'NONE',  ( -2.750000000000000444, 8.729000000000002757, 3.333750000000001990 ) ) ;
#2236=EDGE_LOOP ( 'NONE', ( #4527, #6847, #4036, #622 ) ) ;
#2256=CARTESIAN_POINT ( 'NONE',  ( -2.740000000000000657, 7.969000000000000306, 3.818750000000002753 ) ) ;
#2259=VECTOR ( 'NONE', #506, 39.37007874015748143 ) ;
#2269=CARTESIAN_POINT ( 'NONE',  ( 2.750000000000000888, 8.719000000000001194, 3.333750000000001990 ) ) ;
#2270=AXIS2_PLACEMENT_3D ( 'NONE', #1879, #1961, #1273 ) ;
#2299=FACE_OUTER_BOUND ( 'NONE', #2313, .T. ) ;
#2313=EDGE_LOOP ( 'NONE', ( #2480, #2976, #7988 ) ) ;
#2315=AXIS2_PLACEMENT_3D ( 'NONE', #651, #3608, #6108 ) ;
#2331=DIRECTION ( 'NONE',  ( -0.7071067811865474617, -0.7071067811865474617, -0.000000000000000000 ) ) ;
#2351=DIRECTION ( 'NONE',  ( -0.7071067811865474617, -0.7071067811865474617, -0.000000000000000000 ) ) ;
#2356=CARTESIAN_POINT ( 'NONE',  ( 0.000000000000000000, 7.974000000000001087, 3.323750000000001759 ) ) ;
#2361=LINE ( 'NONE', #4933, #5670 ) ;
#2375=FACE_OUTER_BOUND ( 'NONE', #7389, .T. ) ;
#2382=ORIENTED_EDGE ( 'NONE', *, *, #5480, .F. ) ;
#2386=ORIENTED_EDGE ( 'NONE', *, *, #7832, .T. ) ;
#2399=CARTESIAN_POINT ( 'NONE',  ( -2.750000000000000888, 7.974000000000001087, 3.813750000000002416 ) ) ;
#2400=CARTESIAN_POINT ( 'NONE',  ( 2.750000000000000888, 7.974000000000001087, 3.813750000000002416 ) ) ;
#2404=VECTOR ( 'NONE', #8019, 39.37007874015748854 ) ;
#2410=DIRECTION ( 'NONE',  ( 1.000000000000000000, 0.000000000000000000, 0.000000000000000000 ) ) ;
#2419=VECTOR ( 'NONE', #3912, 39.37007874015748143 ) ;
#2422=VECTOR ( 'NONE', #3809, 39.37007874015748854 ) ;
#2424=ORIENTED_EDGE ( 'NONE', *, *, #5697, .T. ) ;
#2431=CARTESIAN_POINT ( 'NONE',  ( 2.740000000000000657, 7.964000000000000412, 3.813750000000002416 ) ) ;
#2435=LINE ( 'NONE', #5491, #1886 ) ;
#2448=CARTESIAN_POINT ( 'NONE',  ( 2.750000000000000888, 8.719000000000001194, 3.813750000000002416 ) ) ;
#2469=ORIENTED_EDGE ( 'NONE', *, *, #5327, .T. ) ;
#2480=ORIENTED_EDGE ( 'NONE', *, *, #7987, .T. ) ;
#2481=DIRECTION ( 'NONE',  ( -1.000000000000000000, 0.000000000000000000, 0.000000000000000000 ) ) ;
#2482=ORIENTED_EDGE ( 'NONE', *, *, #3533, .F. ) ;
#2488=EDGE_CURVE ( 'NONE', #8018, #7866, #3224, .T. ) ;
#2525=EDGE_CURVE ( 'NONE', #6945, #6736, #3059, .T. ) ;
#2573=ORIENTED_EDGE ( 'NONE', *, *, #6497, .T. ) ;
#2590=ADVANCED_FACE ( 'NONE', ( #5925 ), #5890, .F. ) ;
#2603=ORIENTED_EDGE ( 'NONE', *, *, #3392, .F. ) ;
#2615=DIMENSIONAL_EXPONENTS ( 1.000000000000000000, 0.000000000000000000, 0.000000000000000000, 0.000000000000000000, 0.000000000000000000, 0.000000000000000000, 0.000000000000000000 ) ;
#2629=ADVANCED_FACE ( 'NONE', ( #4693 ), #7209, .F. ) ;
#2635=LINE ( 'NONE', #5086, #323 ) ;
#2639=CARTESIAN_POINT ( 'NONE',  ( -2.740000000000000657, 7.974000000000001087, 3.823750000000002647 ) ) ;
#2645=EDGE_LOOP ( 'NONE', ( #7697, #886, #5653, #1928 ) ) ;
#2646=ADVANCED_FACE ( 'NONE', ( #2854 ), #7248, .T. ) ;
#2651=ORIENTED_EDGE ( 'NONE', *, *, #7420, .F. ) ;
#2659=DIRECTION ( 'NONE',  ( 0.000000000000000000, 0.000000000000000000, 1.000000000000000000 ) ) ;
#2667=ORIENTED_EDGE ( 'NONE', *, *, #7320, .T. ) ;
#2709=CARTESIAN_POINT ( 'NONE',  ( -2.750000000000000888, 7.964000000000000412, 3.333750000000001990 ) ) ;
#2728=ORIENTED_EDGE ( 'NONE', *, *, #5371, .F. ) ;
#2759=DIRECTION ( 'NONE',  ( 0.000000000000000000, 0.000000000000000000, -1.000000000000000000 ) ) ;
#2800=LINE ( 'NONE', #7753, #6725 ) ;
#2812=CARTESIAN_POINT ( 'NONE',  ( 2.740000000000000213, 8.729000000000002757, 3.813750000000002416 ) ) ;
#2854=FACE_OUTER_BOUND ( 'NONE', #7085, .T. ) ;
#2859=CARTESIAN_POINT ( 'NONE',  ( -2.750000000000000444, 8.719000000000001194, 3.333750000000001990 ) ) ;
#2860=CARTESIAN_POINT ( 'NONE',  ( 2.750000000000000888, 8.719000000000001194, 3.333750000000001990 ) ) ;
#2865=EDGE_CURVE ( 'NONE', #822, #4281, #6305, .T. ) ;
#2880=DIRECTION ( 'NONE',  ( -1.000000000000000000, 0.000000000000000000, 0.000000000000000000 ) ) ;
#2899=ORIENTED_EDGE ( 'NONE', *, *, #7153, .T. ) ;
#2909=DESIGN_CONTEXT ( 'detailed design', #4294, 'design' ) ;
#2912=LINE ( 'NONE', #8056, #701 ) ;
#2914=CARTESIAN_POINT ( 'NONE',  ( -2.750000000000000888, 7.974000000000001087, 3.813750000000002416 ) ) ;
#2940=AXIS2_PLACEMENT_3D ( 'NONE', #3715, #1064, #8076 ) ;
#2943=VECTOR ( 'NONE', #7076, 39.37007874015748143 ) ;
#2965=LINE ( 'NONE', #2232, #7673 ) ;
#2976=ORIENTED_EDGE ( 'NONE', *, *, #1426, .T. ) ;
#2985=VERTEX_POINT ( 'NONE', #5889 ) ;
#2987=PLANE ( 'NONE',  #4908 ) ;
#2996=DIRECTION ( 'NONE',  ( -0.7071067811865475727, 0.7071067811865475727, 0.000000000000000000 ) ) ;
#3000=CARTESIAN_POINT ( 'NONE',  ( -2.750000000000000888, 7.974000000000001087, 3.823750000000002647 ) ) ;
#3009=ORIENTED_EDGE ( 'NONE', *, *, #3039, .F. ) ;
#3025=EDGE_LOOP ( 'NONE', ( #1569, #4007, #636, #4563 ) ) ;
#3031=ADVANCED_FACE ( 'NONE', ( #7662 ), #7751, .T. ) ;
#3039=EDGE_CURVE ( 'NONE', #3123, #4445, #419, .T. ) ;
#3056=LINE ( 'NONE', #6215, #7693 ) ;
#3059=LINE ( 'NONE', #3793, #3105 ) ;
#3060=AXIS2_PLACEMENT_3D ( 'NONE', #1131, #6128, #7658 ) ;
#3069=AXIS2_PLACEMENT_3D ( 'NONE', #5884, #3342, #842 ) ;
#3087=CARTESIAN_POINT ( 'NONE',  ( -2.740000000000000213, 8.719000000000001194, 3.823750000000002647 ) ) ;
#3088=EDGE_CURVE ( 'NONE', #4445, #8018, #707, .T. ) ;
#3089=VECTOR ( 'NONE', #4405, 39.37007874015748854 ) ;
#3092=AXIS2_PLACEMENT_3D ( 'NONE', #7897, #7809, #4649 ) ;
#3095=CARTESIAN_POINT ( 'NONE',  ( -2.740000000000000213, 8.719000000000001194, 3.323750000000001759 ) ) ;
#3096=EDGE_CURVE ( 'NONE', #3668, #5577, #1851, .T. ) ;
#3104=EDGE_CURVE ( 'NONE', #822, #6945, #3506, .T. ) ;
#3105=VECTOR ( 'NONE', #1267, 39.37007874015748143 ) ;
#3123=VERTEX_POINT ( 'NONE', #2448 ) ;
#3124=LINE ( 'NONE', #7618, #5842 ) ;
#3151=ORIENTED_EDGE ( 'NONE', *, *, #2865, .T. ) ;
#3223=CARTESIAN_POINT ( 'NONE',  ( -2.740000000000000657, 7.964000000000000412, 3.333750000000001990 ) ) ;
#3224=LINE ( 'NONE', #4946, #2060 ) ;
#3269=CARTESIAN_POINT ( 'NONE',  ( -2.750000000000000888, 7.974000000000001087, 3.823750000000002647 ) ) ;
#3275=CARTESIAN_POINT ( 'NONE',  ( 2.750000000000000888, 7.974000000000001087, 3.333750000000001990 ) ) ;
#3296=LINE ( 'NONE', #7204, #2943 ) ;
#3323=LENGTH_MEASURE_WITH_UNIT ( LENGTH_MEASURE( 0.02539999999999999897 ), #6442 );
#3338=ORIENTED_EDGE ( 'NONE', *, *, #4109, .T. ) ;
#3342=DIRECTION ( 'NONE',  ( 0.7071067811865475727, -0.7071067811865475727, 0.000000000000000000 ) ) ;
#3351=DIRECTION ( 'NONE',  ( 0.000000000000000000, -0.7071067811865475727, 0.7071067811865475727 ) ) ;
#3363=VECTOR ( 'NONE', #7882, 39.37007874015748854 ) ;
#3392=EDGE_CURVE ( 'NONE', #5031, #5123, #3527, .T. ) ;
#3421=PLANE ( 'NONE',  #1910 ) ;
#3435=ORIENTED_EDGE ( 'NONE', *, *, #7374, .T. ) ;
#3448=VECTOR ( 'NONE', #5068, 39.37007874015748854 ) ;
#3494=VECTOR ( 'NONE', #2331, 39.37007874015748854 ) ;
#3506=LINE ( 'NONE', #7202, #6460 ) ;
#3527=LINE ( 'NONE', #7398, #5402 ) ;
#3528=DIRECTION ( 'NONE',  ( -0.7071067811865474617, 0.000000000000000000, 0.7071067811865474617 ) ) ;
#3532=DIRECTION ( 'NONE',  ( -0.000000000000000000, 1.000000000000000000, 0.000000000000000000 ) ) ;
#3533=EDGE_CURVE ( 'NONE', #822, #402, #5769, .T. ) ;
#3542=FACE_OUTER_BOUND ( 'NONE', #5949, .T. ) ;
#3546=DIRECTION ( 'NONE',  ( 0.000000000000000000, 0.000000000000000000, -1.000000000000000000 ) ) ;
#3581=VECTOR ( 'NONE', #297, 39.37007874015748143 ) ;
#3608=DIRECTION ( 'NONE',  ( -0.7071067811865282549, -0.7071067811865668906, 0.000000000000000000 ) ) ;
#3637=ADVANCED_FACE ( 'NONE', ( #4538 ), #1219, .F. ) ;
#3654=DIRECTION ( 'NONE',  ( -0.5773502691896258421, 0.5773502691896258421, 0.5773502691896258421 ) ) ;
#3668=VERTEX_POINT ( 'NONE', #4184 ) ;
#3674=EDGE_LOOP ( 'NONE', ( #2573, #6610, #7316, #507 ) ) ;
#3686=ORIENTED_EDGE ( 'NONE', *, *, #3104, .F. ) ;
#3696=EDGE_CURVE ( 'NONE', #4281, #4445, #2965, .T. ) ;
#3715=CARTESIAN_POINT ( 'NONE',  ( -2.750000000000000444, 8.729000000000002757, 3.333750000000001990 ) ) ;
#3729=ORIENTED_EDGE ( 'NONE', *, *, #4762, .F. ) ;
#3736=CARTESIAN_POINT ( 'NONE',  ( 0.000000000000000000, 0.000000000000000000, 0.000000000000000000 ) ) ;
#3773=PLANE ( 'NONE',  #8007 ) ;
#3789=EDGE_LOOP ( 'NONE', ( #5204, #6885, #2651, #2728 ) ) ;
#3793=CARTESIAN_POINT ( 'NONE',  ( -2.740000000000000657, 7.964000000000000412, 3.823750000000002647 ) ) ;
#3799=EDGE_LOOP ( 'NONE', ( #5384, #1847, #2123 ) ) ;
#3804=ORIENTED_EDGE ( 'NONE', *, *, #7832, .F. ) ;
#3807=CARTESIAN_POINT ( 'NONE',  ( -2.740000000000000213, 8.729000000000002757, 3.333750000000001990 ) ) ;
#3809=DIRECTION ( 'NONE',  ( 0.7071067811865474617, 0.7071067811865474617, -0.000000000000000000 ) ) ;
#3868=DIRECTION ( 'NONE',  ( 0.000000000000000000, -0.000000000000000000, -1.000000000000000000 ) ) ;
#3897=CARTESIAN_POINT ( 'NONE',  ( 2.750000000000000888, 8.719000000000001194, 3.813750000000002416 ) ) ;
#3905=CARTESIAN_POINT ( 'NONE',  ( 2.750000000000000888, 7.964000000000000412, 3.813750000000002416 ) ) ;
#3911=ORIENTED_EDGE ( 'NONE', *, *, #7898, .T. ) ;
#3912=DIRECTION ( 'NONE',  ( -7.142086257945775577E-16, -1.000000000000000000, 0.000000000000000000 ) ) ;
#3920=ORIENTED_EDGE ( 'NONE', *, *, #5708, .T. ) ;
#3923=DIRECTION ( 'NONE',  ( 0.000000000000000000, 1.000000000000000000, 0.000000000000000000 ) ) ;
#3927=VERTEX_POINT ( 'NONE', #2639 ) ;
#3961=VECTOR ( 'NONE', #7429, 39.37007874015748854 ) ;
#3965=( NAMED_UNIT ( * ) PLANE_ANGLE_UNIT ( ) SI_UNIT ( $, .RADIAN. ) );
#3986=LINE ( 'NONE', #2234, #5418 ) ;
#4007=ORIENTED_EDGE ( 'NONE', *, *, #7277, .F. ) ;
#4020=PLANE ( 'NONE',  #211 ) ;
#4033=ORIENTED_EDGE ( 'NONE', *, *, #1523, .T. ) ;
#4036=ORIENTED_EDGE ( 'NONE', *, *, #7898, .F. ) ;
#4043=ORIENTED_EDGE ( 'NONE', *, *, #5327, .F. ) ;
#4051=UNCERTAINTY_MEASURE_WITH_UNIT (LENGTH_MEASURE( 1.000000000000000082E-05 ), #5826, 'distance_accuracy_value', 'NONE');
#4063=DIRECTION ( 'NONE',  ( -1.000000000000000000, 0.000000000000000000, 0.000000000000000000 ) ) ;
#4064=CARTESIAN_POINT ( 'NONE',  ( 2.750000000000000888, 7.964000000000000412, 3.813750000000002416 ) ) ;
#4094=FACE_OUTER_BOUND ( 'NONE', #545, .T. ) ;
#4109=EDGE_CURVE ( 'NONE', #402, #1477, #2190, .T. ) ;
#4116=PLANE ( 'NONE',  #4899 ) ;
#4123=ORIENTED_EDGE ( 'NONE', *, *, #7987, .F. ) ;
#4140=CARTESIAN_POINT ( 'NONE',  ( 2.750000000000000888, 7.964000000000000412, 3.333750000000001990 ) ) ;
#4143=DIRECTION ( 'NONE',  ( -1.000000000000000000, 7.142086257945775577E-16, 0.000000000000000000 ) ) ;
#4162=ADVANCED_BREP_SHAPE_REPRESENTATION ( '', ( #4616, #7272 ), #1120 ) ;
#4165=DIRECTION ( 'NONE',  ( 0.7071067811865554553, 1.586444216266441231E-14, -0.7071067811865394681 ) ) ;
#4174=LINE ( 'NONE', #376, #5195 ) ;
#4180=LINE ( 'NONE', #2914, #2404 ) ;
#4184=CARTESIAN_POINT ( 'NONE',  ( 2.740000000000000657, 8.719000000000001194, 3.323750000000001759 ) ) ;
#4185=DIRECTION ( 'NONE',  ( -7.142086257945775577E-16, -1.000000000000000000, 0.000000000000000000 ) ) ;
#4193=EDGE_CURVE ( 'NONE', #7866, #7102, #2435, .T. ) ;
#4212=AXIS2_PLACEMENT_3D ( 'NONE', #423, #2996, #7285 ) ;
#4213=AXIS2_PLACEMENT_3D ( 'NONE', #2013, #4636, #3532 ) ;
#4230=ORIENTED_EDGE ( 'NONE', *, *, #5558, .T. ) ;
#4265=EDGE_CURVE ( 'NONE', #4344, #7866, #1776, .T. ) ;
#4278=EDGE_CURVE ( 'NONE', #4859, #3123, #8100, .T. ) ;
#4281=VERTEX_POINT ( 'NONE', #4924 ) ;
#4283=CARTESIAN_POINT ( 'NONE',  ( 0.000000000000000000, 0.000000000000000000, 3.823750000000002647 ) ) ;
#4294=APPLICATION_CONTEXT ( 'configuration controlled 3d designs of mechanical parts and assemblies' ) ;
#4308=DIRECTION ( 'NONE',  ( 0.000000000000000000, 0.000000000000000000, 1.000000000000000000 ) ) ;
#4327=CARTESIAN_POINT ( 'NONE',  ( 2.750000000000000888, 7.974000000000001087, 3.333750000000001990 ) ) ;
#4344=VERTEX_POINT ( 'NONE', #3807 ) ;
#4405=DIRECTION ( 'NONE',  ( -0.7071067811865667796, 0.7071067811865281438, -0.000000000000000000 ) ) ;
#4423=FACE_OUTER_BOUND ( 'NONE', #7421, .T. ) ;
#4445=VERTEX_POINT ( 'NONE', #4550 ) ;
#4509=ORIENTED_EDGE ( 'NONE', *, *, #3096, .T. ) ;
#4516=CARTESIAN_POINT ( 'NONE',  ( 2.740000000000000213, 8.724000000000001975, 3.328750000000001652 ) ) ;
#4527=ORIENTED_EDGE ( 'NONE', *, *, #1550, .T. ) ;
#4537=ORIENTED_EDGE ( 'NONE', *, *, #6497, .F. ) ;
#4538=FACE_OUTER_BOUND ( 'NONE', #6320, .T. ) ;
#4546=FACE_OUTER_BOUND ( 'NONE', #7188, .T. ) ;
#4550=CARTESIAN_POINT ( 'NONE',  ( 2.740000000000000657, 8.719000000000001194, 3.823750000000002647 ) ) ;
#4563=ORIENTED_EDGE ( 'NONE', *, *, #3088, .F. ) ;
#4575=ADVANCED_FACE ( 'NONE', ( #2299 ), #4793, .T. ) ;
#4600=ORIENTED_EDGE ( 'NONE', *, *, #5480, .T. ) ;
#4616=MANIFOLD_SOLID_BREP ( 'N', #6353 ) ;
#4636=DIRECTION ( 'NONE',  ( 0.7071067811865475727, 0.000000000000000000, 0.7071067811865475727 ) ) ;
#4649=DIRECTION ( 'NONE',  ( -1.000000000000000000, 0.000000000000000000, -0.000000000000000000 ) ) ;
#4693=FACE_OUTER_BOUND ( 'NONE', #7507, .T. ) ;
#4747=ORIENTED_EDGE ( 'NONE', *, *, #4193, .F. ) ;
#4758=DIRECTION ( 'NONE',  ( 1.000000000000000000, 0.000000000000000000, 0.000000000000000000 ) ) ;
#4762=EDGE_CURVE ( 'NONE', #3927, #4281, #6803, .T. ) ;
#4793=PLANE ( 'NONE',  #1370 ) ;
#4801=AXIS2_PLACEMENT_3D ( 'NONE', #1594, #6598, #6473 ) ;
#4811=CARTESIAN_POINT ( 'NONE',  ( -2.750000000000000888, 7.964000000000000412, 3.823750000000002647 ) ) ;
#4822=EDGE_CURVE ( 'NONE', #8018, #3927, #2048, .T. ) ;
#4826=ORIENTED_EDGE ( 'NONE', *, *, #7420, .T. ) ;
#4840=ORIENTED_EDGE ( 'NONE', *, *, #5427, .T. ) ;
#4841=LINE ( 'NONE', #2256, #3363 ) ;
#4859=VERTEX_POINT ( 'NONE', #1963 ) ;
#4879=VECTOR ( 'NONE', #4758, 39.37007874015748143 ) ;
#4884=ORIENTED_EDGE ( 'NONE', *, *, #2865, .F. ) ;
#4899=AXIS2_PLACEMENT_3D ( 'NONE', #5346, #1518, #282 ) ;
#4908=AXIS2_PLACEMENT_3D ( 'NONE', #5610, #3654, #6149 ) ;
#4916=ORIENTED_EDGE ( 'NONE', *, *, #7320, .F. ) ;
#4921=CARTESIAN_POINT ( 'NONE',  ( -2.745000000000000551, 8.719000000000001194, 3.818750000000002753 ) ) ;
#4924=CARTESIAN_POINT ( 'NONE',  ( 2.740000000000000657, 7.974000000000001087, 3.823750000000002647 ) ) ;
#4933=CARTESIAN_POINT ( 'NONE',  ( 2.740000000000000657, 7.964000000000000412, 3.823750000000002647 ) ) ;
#4941=EDGE_LOOP ( 'NONE', ( #4509, #3435, #4033, #5105 ) ) ;
#4944=LINE ( 'NONE', #4327, #7558 ) ;
#4946=CARTESIAN_POINT ( 'NONE',  ( -2.740000000000000213, 8.729000000000002757, 3.813750000000002416 ) ) ;
#4949=PLANE ( 'NONE',  #7846 ) ;
#4971=ORIENTED_EDGE ( 'NONE', *, *, #2192, .F. ) ;
#4974=DIRECTION ( 'NONE',  ( 0.7071067811865474617, -0.7071067811865474617, 0.000000000000000000 ) ) ;
#4988=PLANE ( 'NONE',  #2315 ) ;
#4990=EDGE_LOOP ( 'NONE', ( #7768, #664, #6503, #2386 ) ) ;
#5008=ORIENTED_EDGE ( 'NONE', *, *, #4822, .T. ) ;
#5021=DIRECTION ( 'NONE',  ( 0.000000000000000000, 0.7071067811865474617, -0.7071067811865474617 ) ) ;
#5031=VERTEX_POINT ( 'NONE', #2859 ) ;
#5044=ADVANCED_FACE ( 'NONE', ( #7129 ), #4116, .T. ) ;
#5057=ORIENTED_EDGE ( 'NONE', *, *, #1550, .F. ) ;
#5068=DIRECTION ( 'NONE',  ( -0.000000000000000000, 0.7071067811865474617, 0.7071067811865474617 ) ) ;
#5072=FACE_OUTER_BOUND ( 'NONE', #2236, .T. ) ;
#5086=CARTESIAN_POINT ( 'NONE',  ( 2.750000000000000888, 8.729000000000002757, 3.333750000000001990 ) ) ;
#5087=ORIENTED_EDGE ( 'NONE', *, *, #2525, .T. ) ;
#5105=ORIENTED_EDGE ( 'NONE', *, *, #2192, .T. ) ;
#5122=LINE ( 'NONE', #2011, #2422 ) ;
#5123=VERTEX_POINT ( 'NONE', #1099 ) ;
#5136=VECTOR ( 'NONE', #2481, 39.37007874015748143 ) ;
#5172=FACE_OUTER_BOUND ( 'NONE', #6114, .T. ) ;
#5177=FACE_OUTER_BOUND ( 'NONE', #396, .T. ) ;
#5195=VECTOR ( 'NONE', #7919, 39.37007874015748854 ) ;
#5204=ORIENTED_EDGE ( 'NONE', *, *, #3039, .T. ) ;
#5222=VERTEX_POINT ( 'NONE', #8161 ) ;
#5240=ORIENTED_EDGE ( 'NONE', *, *, #7277, .T. ) ;
#5245=LINE ( 'NONE', #7798, #4879 ) ;
#5266=DIRECTION ( 'NONE',  ( 7.142086257945775577E-16, 1.000000000000000000, 0.000000000000000000 ) ) ;
#5268=ORIENTED_EDGE ( 'NONE', *, *, #1330, .T. ) ;
#5300=CARTESIAN_POINT ( 'NONE',  ( 2.750000000000000888, 7.964000000000000412, 3.333750000000001990 ) ) ;
#5303=VECTOR ( 'NONE', #7399, 39.37007874015748854 ) ;
#5326=CARTESIAN_POINT ( 'NONE',  ( -2.750000000000000444, 8.719000000000001194, 3.823750000000002647 ) ) ;
#5327=EDGE_CURVE ( 'NONE', #1089, #4344, #3986, .T. ) ;
#5331=VERTEX_POINT ( 'NONE', #2812 ) ;
#5346=CARTESIAN_POINT ( 'NONE',  ( -2.750000000000000444, 8.729000000000002757, 3.813750000000002416 ) ) ;
#5347=DIRECTION ( 'NONE',  ( 0.7071067811865667796, -0.7071067811865281438, -0.000000000000000000 ) ) ;
#5363=DIRECTION ( 'NONE',  ( -0.7071067811865474617, -0.000000000000000000, 0.7071067811865474617 ) ) ;
#5371=EDGE_CURVE ( 'NONE', #3123, #402, #7161, .T. ) ;
#5374=DIRECTION ( 'NONE',  ( -7.142086257945775577E-16, -1.000000000000000000, 0.000000000000000000 ) ) ;
#5384=ORIENTED_EDGE ( 'NONE', *, *, #476, .F. ) ;
#5402=VECTOR ( 'NONE', #4165, 39.37007874015748854 ) ;
#5412=LINE ( 'NONE', #1046, #8080 ) ;
#5418=VECTOR ( 'NONE', #7243, 39.37007874015748143 ) ;
#5427=EDGE_CURVE ( 'NONE', #5331, #1089, #3296, .T. ) ;
#5450=ADVANCED_FACE ( 'NONE', ( #5177 ), #7118, .F. ) ;
#5454=ORIENTED_EDGE ( 'NONE', *, *, #4109, .F. ) ;
#5460=DIRECTION ( 'NONE',  ( -0.000000000000000000, 1.000000000000000000, 0.000000000000000000 ) ) ;
#5480=EDGE_CURVE ( 'NONE', #5222, #822, #2361, .T. ) ;
#5486=SHAPE_DEFINITION_REPRESENTATION ( #100, #6762 ) ;
#5491=CARTESIAN_POINT ( 'NONE',  ( -2.740000000000000213, 8.729000000000002757, 3.813750000000002416 ) ) ;
#5524=ADVANCED_FACE ( 'NONE', ( #8064 ), #1787, .T. ) ;
#5525=DIRECTION ( 'NONE',  ( 7.142086257945775577E-16, 1.000000000000000000, 0.000000000000000000 ) ) ;
#5529=CARTESIAN_POINT ( 'NONE',  ( -2.740000000000000213, 8.729000000000002757, 3.823750000000002647 ) ) ;
#5531=VECTOR ( 'NONE', #305, 39.37007874015748143 ) ;
#5535=ORIENTED_EDGE ( 'NONE', *, *, #942, .F. ) ;
#5558=EDGE_CURVE ( 'NONE', #3668, #4859, #6088, .T. ) ;
#5577=VERTEX_POINT ( 'NONE', #7295 ) ;
#5595=CARTESIAN_POINT ( 'NONE',  ( 2.750000000000000888, 8.729000000000002757, 3.823750000000002647 ) ) ;
#5610=CARTESIAN_POINT ( 'NONE',  ( -2.740000000000000213, 8.729000000000002757, 3.813750000000002416 ) ) ;
#5616=ADVANCED_FACE ( 'NONE', ( #7337 ), #6747, .T. ) ;
#5618=DIRECTION ( 'NONE',  ( 1.000000000000000000, 0.000000000000000000, 0.000000000000000000 ) ) ;
#5625=ORIENTED_EDGE ( 'NONE', *, *, #187, .T. ) ;
#5653=ORIENTED_EDGE ( 'NONE', *, *, #187, .F. ) ;
#5670=VECTOR ( 'NONE', #6670, 39.37007874015748143 ) ;
#5689=CARTESIAN_POINT ( 'NONE',  ( -2.740000000000000657, 7.964000000000000412, 3.823750000000002647 ) ) ;
#5697=EDGE_CURVE ( 'NONE', #5031, #4344, #5122, .T. ) ;
#5708=EDGE_CURVE ( 'NONE', #1477, #4859, #2635, .T. ) ;
#5769=LINE ( 'NONE', #6347, #6617 ) ;
#5798=EDGE_LOOP ( 'NONE', ( #2128, #134, #1820, #5008 ) ) ;
#5801=FACE_OUTER_BOUND ( 'NONE', #1885, .T. ) ;
#5826=( CONVERSION_BASED_UNIT ( 'INCH', #3323 ) LENGTH_UNIT ( ) NAMED_UNIT ( #2615 ) );
#5842=VECTOR ( 'NONE', #5525, 39.37007874015748143 ) ;
#5845=LINE ( 'NONE', #3897, #3089 ) ;
#5884=CARTESIAN_POINT ( 'NONE',  ( -2.740000000000000213, 8.729000000000002757, 3.823750000000002647 ) ) ;
#5889=CARTESIAN_POINT ( 'NONE',  ( -2.750000000000000888, 7.974000000000001087, 3.813750000000002416 ) ) ;
#5890=PLANE ( 'NONE',  #1537 ) ;
#5891=ORIENTED_EDGE ( 'NONE', *, *, #4278, .T. ) ;
#5925=FACE_OUTER_BOUND ( 'NONE', #3674, .T. ) ;
#5949=EDGE_LOOP ( 'NONE', ( #465, #1713, #4123, #1138 ) ) ;
#5970=FACE_OUTER_BOUND ( 'NONE', #4941, .T. ) ;
#5980=LINE ( 'NONE', #7945, #3494 ) ;
#6047=DIRECTION ( 'NONE',  ( 0.7071067811865474617, 0.000000000000000000, 0.7071067811865474617 ) ) ;
#6078=LINE ( 'NONE', #4140, #2259 ) ;
#6081=APPLICATION_CONTEXT ( 'configuration controlled 3d designs of mechanical parts and assemblies' ) ;
#6088=LINE ( 'NONE', #2269, #447 ) ;
#6100=ORIENTED_EDGE ( 'NONE', *, *, #7364, .T. ) ;
#6108=DIRECTION ( 'NONE',  ( 0.000000000000000000, -0.000000000000000000, 1.000000000000000000 ) ) ;
#6114=EDGE_LOOP ( 'NONE', ( #2424, #6995, #2603 ) ) ;
#6128=DIRECTION ( 'NONE',  ( 0.5773502691896152950, 0.5773502691896467143, -0.5773502691896152950 ) ) ;
#6136=ADVANCED_FACE ( 'NONE', ( #497 ), #2987, .T. ) ;
#6148=DIRECTION ( 'NONE',  ( 1.000000000000000000, 0.000000000000000000, 0.000000000000000000 ) ) ;
#6149=DIRECTION ( 'NONE',  ( 0.7071067811865474617, 0.000000000000000000, 0.7071067811865474617 ) ) ;
#6180=DIRECTION ( 'NONE',  ( 0.000000000000000000, -0.7071067811865282549, 0.7071067811865667796 ) ) ;
#6186=LINE ( 'NONE', #4921, #7984 ) ;
#6208=VECTOR ( 'NONE', #5266, 39.37007874015748143 ) ;
#6210=PLANE ( 'NONE',  #1665 ) ;
#6215=CARTESIAN_POINT ( 'NONE',  ( 2.740000000000000657, 7.969000000000000306, 3.328750000000002096 ) ) ;
#6237=DIRECTION ( 'NONE',  ( 0.000000000000000000, 0.000000000000000000, 1.000000000000000000 ) ) ;
#6249=CARTESIAN_POINT ( 'NONE',  ( -2.740000000000000657, 7.964000000000000412, 3.333750000000001990 ) ) ;
#6257=EDGE_LOOP ( 'NONE', ( #5535, #5454, #2482, #2382 ) ) ;
#6264=FACE_OUTER_BOUND ( 'NONE', #2645, .T. ) ;
#6271=DIRECTION ( 'NONE',  ( 0.5773502691896258421, -0.5773502691896258421, 0.5773502691896258421 ) ) ;
#6305=LINE ( 'NONE', #1268, #3448 ) ;
#6320=EDGE_LOOP ( 'NONE', ( #2899, #7993, #2667, #1212 ) ) ;
#6335=VECTOR ( 'NONE', #625, 39.37007874015748143 ) ;
#6347=CARTESIAN_POINT ( 'NONE',  ( 2.740000000000000657, 7.964000000000000412, 3.813750000000002416 ) ) ;
#6353=CLOSED_SHELL ( 'NONE', ( #6908, #2110, #590, #699, #6756, #6850, #1858, #5616, #1784, #2629, #6428, #5450, #5044, #3031, #7298, #1729, #526, #6136, #1454, #2590, #226, #7589, #2646, #4575, #5524, #3637 ) ) ;
#6360=EDGE_CURVE ( 'NONE', #2985, #7102, #1679, .T. ) ;
#6414=CARTESIAN_POINT ( 'NONE',  ( -2.750000000000000444, 8.719000000000001194, 3.813750000000002416 ) ) ;
#6428=ADVANCED_FACE ( 'NONE', ( #2375 ), #6760, .F. ) ;
#6442=( LENGTH_UNIT ( ) NAMED_UNIT ( * ) SI_UNIT ( $, .METRE. ) );
#6447=EDGE_CURVE ( 'NONE', #5577, #1477, #4944, .T. ) ;
#6456=PLANE ( 'NONE',  #1262 ) ;
#6460=VECTOR ( 'NONE', #4063, 39.37007874015748143 ) ;
#6473=DIRECTION ( 'NONE',  ( -0.000000000000000000, 1.000000000000000000, 0.000000000000000000 ) ) ;
#6497=EDGE_CURVE ( 'NONE', #5577, #5222, #3056, .T. ) ;
#6501=CARTESIAN_POINT ( 'NONE',  ( -2.740000000000000213, 8.729000000000002757, 3.813750000000002416 ) ) ;
#6503=ORIENTED_EDGE ( 'NONE', *, *, #6360, .T. ) ;
#6507=AXIS2_PLACEMENT_3D ( 'NONE', #3275, #151, #7056 ) ;
#6531=LINE ( 'NONE', #2709, #1658 ) ;
#6559=PLANE ( 'NONE',  #3092 ) ;
#6598=DIRECTION ( 'NONE',  ( -0.7071067811865475727, -0.000000000000000000, 0.7071067811865475727 ) ) ;
#6602=ORIENTED_EDGE ( 'NONE', *, *, #3104, .T. ) ;
#6610=ORIENTED_EDGE ( 'NONE', *, *, #7364, .F. ) ;
#6613=CARTESIAN_POINT ( 'NONE',  ( -2.750000000000000444, 8.729000000000002757, 3.813750000000002416 ) ) ;
#6617=VECTOR ( 'NONE', #7607, 39.37007874015748854 ) ;
#6663=DIRECTION ( 'NONE',  ( -0.000000000000000000, 1.000000000000000000, 0.000000000000000000 ) ) ;
#6670=DIRECTION ( 'NONE',  ( 0.000000000000000000, 0.000000000000000000, 1.000000000000000000 ) ) ;
#6689=SHAPE_REPRESENTATION_RELATIONSHIP ( 'NONE' , 'NONE' ,  #6762, #4162 ) ;
#6692=VERTEX_POINT ( 'NONE', #136 ) ;
#6718=VECTOR ( 'NONE', #1855, 39.37007874015748143 ) ;
#6722=CARTESIAN_POINT ( 'NONE',  ( 2.750000000000000888, 7.974000000000001087, 3.823750000000002647 ) ) ;
#6725=VECTOR ( 'NONE', #958, 39.37007874015748143 ) ;
#6732=VECTOR ( 'NONE', #6148, 39.37007874015748143 ) ;
#6736=VERTEX_POINT ( 'NONE', #3223 ) ;
#6746=PRODUCT ( 'bench vise4-', 'bench vise4-', '', ( #7273 ) ) ;
#6747=PLANE ( 'NONE',  #3060 ) ;
#6752=AXIS2_PLACEMENT_3D ( 'NONE', #1010, #971, #5374 ) ;
#6756=ADVANCED_FACE ( 'NONE', ( #5801 ), #1387, .T. ) ;
#6760=PLANE ( 'NONE',  #2940 ) ;
#6762=SHAPE_REPRESENTATION ( 'bench vise4-', ( #7272 ), #1120 ) ;
#6765=LINE ( 'NONE', #6837, #5303 ) ;
#6803=LINE ( 'NONE', #6722, #6732 ) ;
#6825=DIRECTION ( 'NONE',  ( 0.000000000000000000, 0.000000000000000000, -1.000000000000000000 ) ) ;
#6837=CARTESIAN_POINT ( 'NONE',  ( 2.740000000000000213, 8.724000000000001975, 3.818750000000003197 ) ) ;
#6847=ORIENTED_EDGE ( 'NONE', *, *, #6360, .F. ) ;
#6850=ADVANCED_FACE ( 'N', ( #5970 ), #6559, .T. ) ;
#6866=FACE_OUTER_BOUND ( 'NONE', #1199, .T. ) ;
#6885=ORIENTED_EDGE ( 'NONE', *, *, #3696, .F. ) ;
#6908=ADVANCED_FACE ( 'NONE', ( #7340 ), #1091, .F. ) ;
#6941=CARTESIAN_POINT ( 'NONE',  ( -2.740000000000000213, 8.719000000000001194, 3.323750000000001759 ) ) ;
#6945=VERTEX_POINT ( 'NONE', #8068 ) ;
#6978=VECTOR ( 'NONE', #2880, 39.37007874015748143 ) ;
#6991=AXIS2_PLACEMENT_3D ( 'NONE', #2399, #389, #6047 ) ;
#6995=ORIENTED_EDGE ( 'NONE', *, *, #7675, .T. ) ;
#7056=DIRECTION ( 'NONE',  ( -0.7071067811865474617, 0.000000000000000000, -0.7071067811865474617 ) ) ;
#7076=DIRECTION ( 'NONE',  ( 0.000000000000000000, 0.000000000000000000, -1.000000000000000000 ) ) ;
#7085=EDGE_LOOP ( 'NONE', ( #3151, #3729, #732, #3686 ) ) ;
#7102=VERTEX_POINT ( 'NONE', #6414 ) ;
#7110=LINE ( 'NONE', #5326, #970 ) ;
#7118=PLANE ( 'NONE',  #3069 ) ;
#7129=FACE_OUTER_BOUND ( 'NONE', #3025, .T. ) ;
#7140=DIRECTION ( 'NONE',  ( -0.5773502691896258421, -0.5773502691896258421, -0.5773502691896258421 ) ) ;
#7145=ORIENTED_EDGE ( 'NONE', *, *, #4265, .F. ) ;
#7153=EDGE_CURVE ( 'NONE', #963, #6736, #757, .T. ) ;
#7160=VECTOR ( 'NONE', #4974, 39.37007874015748854 ) ;
#7161=LINE ( 'NONE', #4064, #2022 ) ;
#7188=EDGE_LOOP ( 'NONE', ( #7881, #7596, #4537 ) ) ;
#7202=CARTESIAN_POINT ( 'NONE',  ( -2.750000000000000888, 7.964000000000000412, 3.813750000000002416 ) ) ;
#7204=CARTESIAN_POINT ( 'NONE',  ( 2.740000000000000213, 8.729000000000002757, 3.823750000000002647 ) ) ;
#7209=PLANE ( 'NONE',  #4801 ) ;
#7242=FACE_OUTER_BOUND ( 'NONE', #4990, .T. ) ;
#7243=DIRECTION ( 'NONE',  ( -1.000000000000000000, 0.000000000000000000, 0.000000000000000000 ) ) ;
#7248=PLANE ( 'NONE',  #7855 ) ;
#7254=VECTOR ( 'NONE', #5363, 39.37007874015748854 ) ;
#7272=AXIS2_PLACEMENT_3D ( 'NONE', #3736, #6237, #5618 ) ;
#7273=MECHANICAL_CONTEXT ( 'NONE', #6081, 'mechanical' ) ;
#7277=EDGE_CURVE ( 'NONE', #7866, #5331, #5245, .T. ) ;
#7285=DIRECTION ( 'NONE',  ( 0.000000000000000000, 0.000000000000000000, -1.000000000000000000 ) ) ;
#7295=CARTESIAN_POINT ( 'NONE',  ( 2.740000000000000657, 7.974000000000001087, 3.323750000000001759 ) ) ;
#7298=ADVANCED_FACE ( 'NONE', ( #7974 ), #1782, .F. ) ;
#7316=ORIENTED_EDGE ( 'NONE', *, *, #1426, .F. ) ;
#7320=EDGE_CURVE ( 'NONE', #6945, #2985, #4180, .T. ) ;
#7337=FACE_OUTER_BOUND ( 'NONE', #3799, .T. ) ;
#7340=FACE_OUTER_BOUND ( 'NONE', #5798, .T. ) ;
#7347=ORIENTED_EDGE ( 'NONE', *, *, #2488, .T. ) ;
#7349=DIRECTION ( 'NONE',  ( 0.000000000000000000, -0.7071067811865474617, 0.7071067811865474617 ) ) ;
#7364=EDGE_CURVE ( 'NONE', #6736, #5222, #6078, .T. ) ;
#7374=EDGE_CURVE ( 'NONE', #5577, #6692, #384, .T. ) ;
#7388=CARTESIAN_POINT ( 'NONE',  ( -2.750000000000000888, 7.974000000000001087, 3.333750000000001990 ) ) ;
#7389=EDGE_LOOP ( 'NONE', ( #2071, #4971, #1808, #4043 ) ) ;
#7398=CARTESIAN_POINT ( 'NONE',  ( -2.740000000000000213, 8.719000000000001194, 3.323750000000001759 ) ) ;
#7399=DIRECTION ( 'NONE',  ( -3.865154999631033652E-14, 0.7071067811865474617, -0.7071067811865474617 ) ) ;
#7420=EDGE_CURVE ( 'NONE', #402, #4281, #5412, .T. ) ;
#7421=EDGE_LOOP ( 'NONE', ( #436, #4826, #4884 ) ) ;
#7429=DIRECTION ( 'NONE',  ( -0.000000000000000000, -0.7071067811865474617, -0.7071067811865474617 ) ) ;
#7459=DIRECTION ( 'NONE',  ( -0.7071067811865554553, -1.586444216266441231E-14, -0.7071067811865394681 ) ) ;
#7486=DIRECTION ( 'NONE',  ( 0.7071067811865474617, -0.000000000000000000, 0.7071067811865474617 ) ) ;
#7507=EDGE_LOOP ( 'NONE', ( #4230, #1126, #1815, #1204 ) ) ;
#7528=PLANE ( 'NONE',  #2270 ) ;
#7547=AXIS2_PLACEMENT_3D ( 'NONE', #3269, #142, #2659 ) ;
#7558=VECTOR ( 'NONE', #7486, 39.37007874015748854 ) ;
#7589=ADVANCED_FACE ( 'NONE', ( #5072 ), #7528, .T. ) ;
#7596=ORIENTED_EDGE ( 'NONE', *, *, #942, .T. ) ;
#7607=DIRECTION ( 'NONE',  ( 0.7071067811865474617, 0.7071067811865474617, -0.000000000000000000 ) ) ;
#7617=EDGE_LOOP ( 'NONE', ( #7347, #1100, #5057 ) ) ;
#7618=CARTESIAN_POINT ( 'NONE',  ( -2.740000000000006430, 1.956931634677146971E-15, 3.323750000000001759 ) ) ;
#7630=LINE ( 'NONE', #4516, #1255 ) ;
#7658=DIRECTION ( 'NONE',  ( 0.000000000000000000, 0.7071067811865282549, 0.7071067811865667796 ) ) ;
#7662=FACE_OUTER_BOUND ( 'NONE', #3789, .T. ) ;
#7673=VECTOR ( 'NONE', #5460, 39.37007874015748143 ) ;
#7675=EDGE_CURVE ( 'NONE', #4344, #5123, #8022, .T. ) ;
#7693=VECTOR ( 'NONE', #7349, 39.37007874015748854 ) ;
#7697=ORIENTED_EDGE ( 'NONE', *, *, #1005, .F. ) ;
#7714=DIRECTION ( 'NONE',  ( -0.5773502691896258421, 0.5773502691896258421, -0.5773502691896258421 ) ) ;
#7751=PLANE ( 'NONE',  #4213 ) ;
#7753=CARTESIAN_POINT ( 'NONE',  ( -2.750000000000000888, 7.974000000000001087, 3.813750000000002416 ) ) ;
#7754=DIRECTION ( 'NONE',  ( 3.865154999631033652E-14, -0.7071067811865474617, -0.7071067811865474617 ) ) ;
#7768=ORIENTED_EDGE ( 'NONE', *, *, #1704, .T. ) ;
#7776=EDGE_CURVE ( 'NONE', #963, #2985, #509, .T. ) ;
#7798=CARTESIAN_POINT ( 'NONE',  ( 2.750000000000000888, 8.729000000000002757, 3.813750000000002416 ) ) ;
#7809=DIRECTION ( 'NONE',  ( 0.000000000000000000, 0.000000000000000000, -1.000000000000000000 ) ) ;
#7832=EDGE_CURVE ( 'NONE', #7102, #5031, #7110, .T. ) ;
#7846=AXIS2_PLACEMENT_3D ( 'NONE', #1184, #1761, #6180 ) ;
#7852=CARTESIAN_POINT ( 'NONE',  ( 2.740000000000000657, 0.000000000000000000, 3.323750000000001759 ) ) ;
#7853=PLANE ( 'NONE',  #6752 ) ;
#7855=AXIS2_PLACEMENT_3D ( 'NONE', #3905, #3351, #2160 ) ;
#7866=VERTEX_POINT ( 'NONE', #6501 ) ;
#7881=ORIENTED_EDGE ( 'NONE', *, *, #6447, .T. ) ;
#7882=DIRECTION ( 'NONE',  ( 0.000000000000000000, 0.7071067811865474617, 0.7071067811865474617 ) ) ;
#7897=CARTESIAN_POINT ( 'NONE',  ( 0.000000000000000000, 0.000000000000000000, 3.323750000000001759 ) ) ;
#7898=EDGE_CURVE ( 'NONE', #3927, #2985, #2800, .T. ) ;
#7919=DIRECTION ( 'NONE',  ( -0.000000000000000000, -0.7071067811865474617, 0.7071067811865474617 ) ) ;
#7945=CARTESIAN_POINT ( 'NONE',  ( 2.750000000000000888, 7.974000000000001087, 3.333750000000001990 ) ) ;
#7957=VECTOR ( 'NONE', #4308, 39.37007874015748143 ) ;
#7964=CARTESIAN_POINT ( 'NONE',  ( 2.750000000000000888, 8.719000000000001194, 3.813750000000002416 ) ) ;
#7970=AXIS2_PLACEMENT_3D ( 'NONE', #186, #1338, #3868 ) ;
#7974=FACE_OUTER_BOUND ( 'NONE', #6257, .T. ) ;
#7983=DIRECTION ( 'NONE',  ( -1.000000000000000000, 0.000000000000000000, -0.000000000000000000 ) ) ;
#7984=VECTOR ( 'NONE', #7459, 39.37007874015748854 ) ;
#7987=EDGE_CURVE ( 'NONE', #963, #6692, #2912, .T. ) ;
#7988=ORIENTED_EDGE ( 'NONE', *, *, #7153, .F. ) ;
#7993=ORIENTED_EDGE ( 'NONE', *, *, #2525, .F. ) ;
#8007=AXIS2_PLACEMENT_3D ( 'NONE', #2431, #6271, #658 ) ;
#8015=DIRECTION ( 'NONE',  ( 0.7071067811865554553, -1.583668658704876446E-14, -0.7071067811865395791 ) ) ;
#8018=VERTEX_POINT ( 'NONE', #3087 ) ;
#8019=DIRECTION ( 'NONE',  ( -0.7071067811865474617, 0.7071067811865474617, 0.000000000000000000 ) ) ;
#8022=LINE ( 'NONE', #3095, #3961 ) ;
#8056=CARTESIAN_POINT ( 'NONE',  ( -2.745000000000000995, 7.974000000000001087, 3.328750000000002096 ) ) ;
#8058=DIRECTION ( 'NONE',  ( -0.7071067811865474617, 0.000000000000000000, 0.7071067811865474617 ) ) ;
#8060=ORIENTED_EDGE ( 'NONE', *, *, #5697, .F. ) ;
#8064=FACE_OUTER_BOUND ( 'NONE', #1769, .T. ) ;
#8068=CARTESIAN_POINT ( 'NONE',  ( -2.740000000000000657, 7.964000000000000412, 3.813750000000002416 ) ) ;
#8076=DIRECTION ( 'NONE',  ( -1.000000000000000000, 0.000000000000000000, 0.000000000000000000 ) ) ;
#8080=VECTOR ( 'NONE', #8058, 39.37007874015748854 ) ;
#8100=LINE ( 'NONE', #1731, #6335 ) ;
#8161=CARTESIAN_POINT ( 'NONE',  ( 2.740000000000000657, 7.964000000000000412, 3.333750000000001990 ) ) ;
#8234=COLOUR_RGB('Black', 0.09019608, 0.27058824, 0.51372549);
#8235=FILL_AREA_STYLE_COLOUR('',#8234);
#8236=FILL_AREA_STYLE('',(#8235));
#8237=SURFACE_STYLE_FILL_AREA(#8236);
#8238=SURFACE_SIDE_STYLE('',(#8237));
#8239=SURFACE_STYLE_USAGE(.BOTH.,#8238);
#8240=PRESENTATION_STYLE_ASSIGNMENT((#8239));
#8251=STYLED_ITEM('',(#8240),#4616);
#8252=MECHANICAL_DESIGN_GEOMETRIC_PRESENTATION_REPRESENTATION('',(#8251),#1120);
ENDSEC;
END-ISO-10303-21;
